ISO-10303-21;
HEADER;
/* Generated by software containing ST-Developer
 * from STEP Tools, Inc. (www.steptools.com) 
 */

FILE_DESCRIPTION(
/* description */ ('Wall-mounted air drop station'),
/* implementation_level */ '2;1');

FILE_NAME(
/* name */ 'Valve port reducer (1).step',
/* time_stamp */ '2026-10-28T22:16:19-07:00',
/* author */ (''),
/* organization */ (''),
/* preprocessor_version */ 'ST-DEVELOPER v20.2',
/* originating_system */ 'Autodesk Translation Framework v15.17.0.0',
/* authorisation */ '');

FILE_SCHEMA (('AUTOMOTIVE_DESIGN { 1 0 10303 214 3 1 1 }'));
ENDSEC;

DATA;
#10=MECHANICAL_DESIGN_GEOMETRIC_PRESENTATION_REPRESENTATION('',(#345),#10517);
#287=SHAPE_REPRESENTATION_RELATIONSHIP('SRR','None',#10644,#316);
#316=ADVANCED_BREP_SHAPE_REPRESENTATION('',(#374),#10488);
#345=STYLED_ITEM('',(#10860),#374);
#374=MANIFOLD_SOLID_BREP('Body1',#5884);
#403=FACE_BOUND('',#1124,.T.);
#404=FACE_BOUND('',#1127,.T.);
#405=FACE_BOUND('',#1131,.T.);
#406=FACE_BOUND('',#1133,.T.);
#530=PLANE('',#6258);
#531=PLANE('',#6263);
#532=PLANE('',#6269);
#533=PLANE('',#6270);
#763=FACE_OUTER_BOUND('',#1122,.T.);
#764=FACE_OUTER_BOUND('',#1123,.T.);
#765=FACE_OUTER_BOUND('',#1125,.T.);
#766=FACE_OUTER_BOUND('',#1126,.T.);
#767=FACE_OUTER_BOUND('',#1128,.T.);
#768=FACE_OUTER_BOUND('',#1129,.T.);
#769=FACE_OUTER_BOUND('',#1130,.T.);
#770=FACE_OUTER_BOUND('',#1132,.T.);
#1122=EDGE_LOOP('',(#3997,#3998,#3999,#4000));
#1123=EDGE_LOOP('',(#4001));
#1124=EDGE_LOOP('',(#4002));
#1125=EDGE_LOOP('',(#4003,#4004,#4005,#4006));
#1126=EDGE_LOOP('',(#4007));
#1127=EDGE_LOOP('',(#4008));
#1128=EDGE_LOOP('',(#4009,#4010,#4011,#4012));
#1129=EDGE_LOOP('',(#4013,#4014,#4015,#4016));
#1130=EDGE_LOOP('',(#4017));
#1131=EDGE_LOOP('',(#4018));
#1132=EDGE_LOOP('',(#4019));
#1133=EDGE_LOOP('',(#4020));
#1596=LINE('',#8802,#2060);
#1597=LINE('',#8811,#2061);
#1598=LINE('',#8817,#2062);
#1599=LINE('',#8822,#2063);
#2060=VECTOR('',#6972,0.685);
#2061=VECTOR('',#6983,1.065);
#2062=VECTOR('',#6992,0.46);
#2063=VECTOR('',#6997,1.5);
#2528=CIRCLE('',#6256,0.685);
#2529=CIRCLE('',#6257,0.685);
#2530=CIRCLE('',#6259,0.46);
#2531=CIRCLE('',#6261,1.065);
#2532=CIRCLE('',#6262,1.065);
#2533=CIRCLE('',#6264,0.46);
#2534=CIRCLE('',#6267,1.5);
#2535=CIRCLE('',#6268,1.5);
#2773=VERTEX_POINT('',#8799);
#2774=VERTEX_POINT('',#8801);
#2775=VERTEX_POINT('',#8805);
#2776=VERTEX_POINT('',#8808);
#2777=VERTEX_POINT('',#8810);
#2778=VERTEX_POINT('',#8814);
#2779=VERTEX_POINT('',#8819);
#2780=VERTEX_POINT('',#8821);
#3256=EDGE_CURVE('',#2773,#2773,#2528,.T.);
#3257=EDGE_CURVE('',#2773,#2774,#1596,.T.);
#3258=EDGE_CURVE('',#2774,#2774,#2529,.T.);
#3259=EDGE_CURVE('',#2775,#2775,#2530,.T.);
#3260=EDGE_CURVE('',#2776,#2776,#2531,.T.);
#3261=EDGE_CURVE('',#2776,#2777,#1597,.T.);
#3262=EDGE_CURVE('',#2777,#2777,#2532,.T.);
#3263=EDGE_CURVE('',#2778,#2778,#2533,.T.);
#3264=EDGE_CURVE('',#2775,#2778,#1598,.T.);
#3265=EDGE_CURVE('',#2779,#2779,#2534,.T.);
#3266=EDGE_CURVE('',#2779,#2780,#1599,.T.);
#3267=EDGE_CURVE('',#2780,#2780,#2535,.T.);
#3997=ORIENTED_EDGE('',*,*,#3256,.F.);
#3998=ORIENTED_EDGE('',*,*,#3257,.T.);
#3999=ORIENTED_EDGE('',*,*,#3258,.F.);
#4000=ORIENTED_EDGE('',*,*,#3257,.F.);
#4001=ORIENTED_EDGE('',*,*,#3256,.T.);
#4002=ORIENTED_EDGE('',*,*,#3259,.F.);
#4003=ORIENTED_EDGE('',*,*,#3260,.F.);
#4004=ORIENTED_EDGE('',*,*,#3261,.T.);
#4005=ORIENTED_EDGE('',*,*,#3262,.T.);
#4006=ORIENTED_EDGE('',*,*,#3261,.F.);
#4007=ORIENTED_EDGE('',*,*,#3262,.F.);
#4008=ORIENTED_EDGE('',*,*,#3263,.F.);
#4009=ORIENTED_EDGE('',*,*,#3259,.T.);
#4010=ORIENTED_EDGE('',*,*,#3264,.T.);
#4011=ORIENTED_EDGE('',*,*,#3263,.T.);
#4012=ORIENTED_EDGE('',*,*,#3264,.F.);
#4013=ORIENTED_EDGE('',*,*,#3265,.F.);
#4014=ORIENTED_EDGE('',*,*,#3266,.T.);
#4015=ORIENTED_EDGE('',*,*,#3267,.T.);
#4016=ORIENTED_EDGE('',*,*,#3266,.F.);
#4017=ORIENTED_EDGE('',*,*,#3265,.T.);
#4018=ORIENTED_EDGE('',*,*,#3258,.T.);
#4019=ORIENTED_EDGE('',*,*,#3267,.F.);
#4020=ORIENTED_EDGE('',*,*,#3260,.T.);
#5435=CYLINDRICAL_SURFACE('',#6255,0.685);
#5436=CYLINDRICAL_SURFACE('',#6260,1.065);
#5437=CYLINDRICAL_SURFACE('',#6265,0.46);
#5438=CYLINDRICAL_SURFACE('',#6266,1.5);
#5536=ADVANCED_FACE('',(#763),#5435,.F.);
#5537=ADVANCED_FACE('',(#764,#403),#530,.T.);
#5538=ADVANCED_FACE('',(#765),#5436,.F.);
#5539=ADVANCED_FACE('',(#766,#404),#531,.F.);
#5540=ADVANCED_FACE('',(#767),#5437,.F.);
#5541=ADVANCED_FACE('',(#768),#5438,.T.);
#5542=ADVANCED_FACE('',(#769,#405),#532,.T.);
#5543=ADVANCED_FACE('',(#770,#406),#533,.F.);
#5884=CLOSED_SHELL('',(#5536,#5537,#5538,#5539,#5540,#5541,#5542,#5543));
#6254=AXIS2_PLACEMENT_3D('',#8797,#6966,#6967);
#6255=AXIS2_PLACEMENT_3D('',#8798,#6968,#6969);
#6256=AXIS2_PLACEMENT_3D('',#8800,#6970,#6971);
#6257=AXIS2_PLACEMENT_3D('',#8803,#6973,#6974);
#6258=AXIS2_PLACEMENT_3D('',#8804,#6975,#6976);
#6259=AXIS2_PLACEMENT_3D('',#8806,#6977,#6978);
#6260=AXIS2_PLACEMENT_3D('',#8807,#6979,#6980);
#6261=AXIS2_PLACEMENT_3D('',#8809,#6981,#6982);
#6262=AXIS2_PLACEMENT_3D('',#8812,#6984,#6985);
#6263=AXIS2_PLACEMENT_3D('',#8813,#6986,#6987);
#6264=AXIS2_PLACEMENT_3D('',#8815,#6988,#6989);
#6265=AXIS2_PLACEMENT_3D('',#8816,#6990,#6991);
#6266=AXIS2_PLACEMENT_3D('',#8818,#6993,#6994);
#6267=AXIS2_PLACEMENT_3D('',#8820,#6995,#6996);
#6268=AXIS2_PLACEMENT_3D('',#8823,#6998,#6999);
#6269=AXIS2_PLACEMENT_3D('',#8824,#7000,#7001);
#6270=AXIS2_PLACEMENT_3D('',#8825,#7002,#7003);
#6966=DIRECTION('axis',(0.,0.,1.));
#6967=DIRECTION('refdir',(1.,0.,0.));
#6968=DIRECTION('center_axis',(0.,1.,0.));
#6969=DIRECTION('ref_axis',(1.,0.,0.));
#6970=DIRECTION('center_axis',(0.,1.,0.));
#6971=DIRECTION('ref_axis',(1.,0.,0.));
#6972=DIRECTION('',(0.,1.,0.));
#6973=DIRECTION('center_axis',(0.,-1.,0.));
#6974=DIRECTION('ref_axis',(1.,0.,0.));
#6975=DIRECTION('center_axis',(0.,1.,0.));
#6976=DIRECTION('ref_axis',(1.,0.,0.));
#6977=DIRECTION('center_axis',(0.,1.,0.));
#6978=DIRECTION('ref_axis',(1.,0.,0.));
#6979=DIRECTION('center_axis',(0.,1.,0.));
#6980=DIRECTION('ref_axis',(1.,0.,0.));
#6981=DIRECTION('center_axis',(0.,1.,0.));
#6982=DIRECTION('ref_axis',(1.,0.,0.));
#6983=DIRECTION('',(0.,1.,0.));
#6984=DIRECTION('center_axis',(0.,1.,0.));
#6985=DIRECTION('ref_axis',(1.,0.,0.));
#6986=DIRECTION('center_axis',(0.,1.,0.));
#6987=DIRECTION('ref_axis',(1.,0.,0.));
#6988=DIRECTION('center_axis',(0.,-1.,0.));
#6989=DIRECTION('ref_axis',(1.,0.,0.));
#6990=DIRECTION('center_axis',(0.,1.,0.));
#6991=DIRECTION('ref_axis',(1.,0.,0.));
#6992=DIRECTION('',(0.,-1.,0.));
#6993=DIRECTION('center_axis',(0.,1.,0.));
#6994=DIRECTION('ref_axis',(1.,0.,0.));
#6995=DIRECTION('center_axis',(0.,1.,0.));
#6996=DIRECTION('ref_axis',(1.,0.,0.));
#6997=DIRECTION('',(0.,-1.,0.));
#6998=DIRECTION('center_axis',(0.,1.,0.));
#6999=DIRECTION('ref_axis',(1.,0.,0.));
#7000=DIRECTION('center_axis',(0.,1.,0.));
#7001=DIRECTION('ref_axis',(1.,0.,0.));
#7002=DIRECTION('center_axis',(0.,1.,0.));
#7003=DIRECTION('ref_axis',(1.,0.,0.));
#8797=CARTESIAN_POINT('',(0.,0.,0.));
#8798=CARTESIAN_POINT('Origin',(0.,7.3,5.));
#8799=CARTESIAN_POINT('',(-0.685,7.3,5.));
#8800=CARTESIAN_POINT('Origin',(0.,7.3,5.));
#8801=CARTESIAN_POINT('',(-0.685,8.5,5.));
#8802=CARTESIAN_POINT('',(-0.685,7.3,5.));
#8803=CARTESIAN_POINT('Origin',(0.,8.5,5.));
#8804=CARTESIAN_POINT('Origin',(0.,7.3,5.));
#8805=CARTESIAN_POINT('',(-0.46,7.3,5.));
#8806=CARTESIAN_POINT('Origin',(0.,7.3,5.));
#8807=CARTESIAN_POINT('Origin',(0.,5.4,5.));
#8808=CARTESIAN_POINT('',(-1.065,5.5,5.));
#8809=CARTESIAN_POINT('Origin',(0.,5.5,5.));
#8810=CARTESIAN_POINT('',(-1.065,7.,5.));
#8811=CARTESIAN_POINT('',(-1.065,5.4,5.));
#8812=CARTESIAN_POINT('Origin',(0.,7.,5.));
#8813=CARTESIAN_POINT('Origin',(0.,7.,5.));
#8814=CARTESIAN_POINT('',(-0.46,7.,5.));
#8815=CARTESIAN_POINT('Origin',(0.,7.,5.));
#8816=CARTESIAN_POINT('Origin',(0.,5.5,5.));
#8817=CARTESIAN_POINT('',(-0.46,5.5,5.));
#8818=CARTESIAN_POINT('Origin',(0.,5.5,5.));
#8819=CARTESIAN_POINT('',(-1.5,8.5,5.));
#8820=CARTESIAN_POINT('Origin',(0.,8.5,5.));
#8821=CARTESIAN_POINT('',(-1.5,5.5,5.));
#8822=CARTESIAN_POINT('',(-1.5,5.5,5.));
#8823=CARTESIAN_POINT('Origin',(0.,5.5,5.));
#8824=CARTESIAN_POINT('Origin',(0.,8.5,5.));
#8825=CARTESIAN_POINT('Origin',(0.,5.5,5.));
#10455=UNCERTAINTY_MEASURE_WITH_UNIT(LENGTH_MEASURE(0.001),#10518,
'DISTANCE_ACCURACY_VALUE',
'Maximum model space distance between geometric entities at asserted c
onnectivities');
#10484=UNCERTAINTY_MEASURE_WITH_UNIT(LENGTH_MEASURE(0.001),#10518,
'DISTANCE_ACCURACY_VALUE',
'Maximum model space distance between geometric entities at asserted c
onnectivities');
#10488=(
GEOMETRIC_REPRESENTATION_CONTEXT(3)
GLOBAL_UNCERTAINTY_ASSIGNED_CONTEXT((#10455))
GLOBAL_UNIT_ASSIGNED_CONTEXT((#10518,#10520,#10521))
REPRESENTATION_CONTEXT('','3D')
);
#10517=(
GEOMETRIC_REPRESENTATION_CONTEXT(3)
GLOBAL_UNCERTAINTY_ASSIGNED_CONTEXT((#10484))
GLOBAL_UNIT_ASSIGNED_CONTEXT((#10518,#10520,#10521))
REPRESENTATION_CONTEXT('','3D')
);
#10518=(
LENGTH_UNIT()
NAMED_UNIT(*)
SI_UNIT(.CENTI.,.METRE.)
);
#10520=(
NAMED_UNIT(*)
PLANE_ANGLE_UNIT()
SI_UNIT($,.RADIAN.)
);
#10521=(
NAMED_UNIT(*)
SI_UNIT($,.STERADIAN.)
SOLID_ANGLE_UNIT()
);
#10525=SHAPE_DEFINITION_REPRESENTATION(#10557,#10644);
#10557=PRODUCT_DEFINITION_SHAPE('',$,#10677);
#10644=SHAPE_REPRESENTATION('',(#6254),#10488);
#10673=PRODUCT_DEFINITION_CONTEXT('part definition',#10771,'design');
#10677=PRODUCT_DEFINITION('Valve port reducer (1)',
'Valve port reducer (1)',#10709,#10673);
#10709=PRODUCT_DEFINITION_FORMATION('',$,#10776);
#10771=APPLICATION_CONTEXT(
'Core Data for Automotive Mechanical Design Process');
#10772=PRODUCT_CONTEXT('part definition',#10771,'mechanical');
#10776=PRODUCT('Valve port reducer (1)','Valve port reducer (1)',
'Valve port reducer (1)',(#10772));
#10854=COLOUR_RGB('Light Blue',0.38,0.62,0.78);
#10855=FILL_AREA_STYLE_COLOUR('',#10854);
#10856=FILL_AREA_STYLE('',(#10855));
#10857=SURFACE_STYLE_FILL_AREA(#10856);
#10858=SURFACE_SIDE_STYLE('',(#10857));
#10859=SURFACE_STYLE_USAGE(.BOTH.,#10858);
#10860=PRESENTATION_STYLE_ASSIGNMENT((#10859));
ENDSEC;
END-ISO-10303-21;
